ISO-10303-21;
HEADER;
/* Generated by software containing ST-Developer
 * from STEP Tools, Inc. (www.steptools.com) 
 */

FILE_DESCRIPTION(
/* description */ ('Wall-mounted air drop station'),
/* implementation_level */ '2;1');

FILE_NAME(
/* name */ 'Hex Bolt - M6 x 30 mm.step',
/* time_stamp */ '2026-10-28T22:16:19-07:00',
/* author */ (''),
/* organization */ (''),
/* preprocessor_version */ 'ST-DEVELOPER v20.2',
/* originating_system */ 'Autodesk Translation Framework v15.17.0.0',
/* authorisation */ '');

FILE_SCHEMA (('AUTOMOTIVE_DESIGN { 1 0 10303 214 3 1 1 }'));
ENDSEC;

DATA;
#10=MECHANICAL_DESIGN_GEOMETRIC_PRESENTATION_REPRESENTATION('',(#366),#10517);
#245=(
BOUNDED_CURVE()
B_SPLINE_CURVE(2,(#10055,#10056,#10057),.UNSPECIFIED.,.F.,.F.)
B_SPLINE_CURVE_WITH_KNOTS((3,3),(0.144988513094728,0.791574906712449),
 .UNSPECIFIED.)
CURVE()
GEOMETRIC_REPRESENTATION_ITEM()
RATIONAL_B_SPLINE_CURVE((1.09282032302755,1.26188021535082,1.09282032302931))
REPRESENTATION_ITEM('')
);
#246=(
BOUNDED_CURVE()
B_SPLINE_CURVE(2,(#10059,#10060,#10061),.UNSPECIFIED.,.F.,.F.)
B_SPLINE_CURVE_WITH_KNOTS((3,3),(0.144988513094728,0.791574906712449),
 .UNSPECIFIED.)
CURVE()
GEOMETRIC_REPRESENTATION_ITEM()
RATIONAL_B_SPLINE_CURVE((1.09282032302755,1.26188021535082,1.09282032302931))
REPRESENTATION_ITEM('')
);
#247=(
BOUNDED_CURVE()
B_SPLINE_CURVE(2,(#10063,#10064,#10065),.UNSPECIFIED.,.F.,.F.)
B_SPLINE_CURVE_WITH_KNOTS((3,3),(0.144988513094728,0.791574906712449),
 .UNSPECIFIED.)
CURVE()
GEOMETRIC_REPRESENTATION_ITEM()
RATIONAL_B_SPLINE_CURVE((1.09282032302755,1.26188021535082,1.09282032302931))
REPRESENTATION_ITEM('')
);
#248=(
BOUNDED_CURVE()
B_SPLINE_CURVE(2,(#10067,#10068,#10069),.UNSPECIFIED.,.F.,.F.)
B_SPLINE_CURVE_WITH_KNOTS((3,3),(0.144988513094728,0.791574906712449),
 .UNSPECIFIED.)
CURVE()
GEOMETRIC_REPRESENTATION_ITEM()
RATIONAL_B_SPLINE_CURVE((1.09282032302755,1.26188021535082,1.09282032302931))
REPRESENTATION_ITEM('')
);
#249=(
BOUNDED_CURVE()
B_SPLINE_CURVE(2,(#10071,#10072,#10073),.UNSPECIFIED.,.F.,.F.)
B_SPLINE_CURVE_WITH_KNOTS((3,3),(0.144988513094728,0.791574906712449),
 .UNSPECIFIED.)
CURVE()
GEOMETRIC_REPRESENTATION_ITEM()
RATIONAL_B_SPLINE_CURVE((1.09282032302755,1.26188021535082,1.09282032302931))
REPRESENTATION_ITEM('')
);
#250=(
BOUNDED_CURVE()
B_SPLINE_CURVE(2,(#10074,#10075,#10076),.UNSPECIFIED.,.F.,.F.)
B_SPLINE_CURVE_WITH_KNOTS((3,3),(0.144988513094727,0.791574906712449),
 .UNSPECIFIED.)
CURVE()
GEOMETRIC_REPRESENTATION_ITEM()
RATIONAL_B_SPLINE_CURVE((1.09282032302755,1.26188021535082,1.09282032302931))
REPRESENTATION_ITEM('')
);
#281=CONICAL_SURFACE('',#6753,0.27,0.785398163397448);
#282=CONICAL_SURFACE('',#6756,0.576175134594813,1.0471975511966);
#308=SHAPE_REPRESENTATION_RELATIONSHIP('SRR','None',#10665,#337);
#337=ADVANCED_BREP_SHAPE_REPRESENTATION('',(#393),#10509);
#366=STYLED_ITEM('',(#10881),#393);
#393=MANIFOLD_SOLID_BREP('Body1',#5907);
#516=FACE_BOUND('',#1517,.T.);
#692=PLANE('',#6755);
#693=PLANE('',#6758);
#694=PLANE('',#6759);
#695=PLANE('',#6760);
#696=PLANE('',#6761);
#697=PLANE('',#6762);
#698=PLANE('',#6763);
#699=PLANE('',#6764);
#700=PLANE('',#6765);
#1033=FACE_OUTER_BOUND('',#1505,.T.);
#1034=FACE_OUTER_BOUND('',#1506,.T.);
#1035=FACE_OUTER_BOUND('',#1507,.T.);
#1036=FACE_OUTER_BOUND('',#1508,.T.);
#1037=FACE_OUTER_BOUND('',#1509,.T.);
#1038=FACE_OUTER_BOUND('',#1510,.T.);
#1039=FACE_OUTER_BOUND('',#1511,.T.);
#1040=FACE_OUTER_BOUND('',#1512,.T.);
#1041=FACE_OUTER_BOUND('',#1513,.T.);
#1042=FACE_OUTER_BOUND('',#1514,.T.);
#1043=FACE_OUTER_BOUND('',#1515,.T.);
#1044=FACE_OUTER_BOUND('',#1516,.T.);
#1505=EDGE_LOOP('',(#5111,#5112,#5113,#5114));
#1506=EDGE_LOOP('',(#5115,#5116,#5117,#5118));
#1507=EDGE_LOOP('',(#5119));
#1508=EDGE_LOOP('',(#5120,#5121,#5122,#5123,#5124,#5125,#5126,#5127,#5128));
#1509=EDGE_LOOP('',(#5129,#5130,#5131,#5132));
#1510=EDGE_LOOP('',(#5133,#5134,#5135,#5136));
#1511=EDGE_LOOP('',(#5137,#5138,#5139,#5140));
#1512=EDGE_LOOP('',(#5141,#5142,#5143,#5144));
#1513=EDGE_LOOP('',(#5145,#5146,#5147,#5148));
#1514=EDGE_LOOP('',(#5149,#5150,#5151,#5152));
#1515=EDGE_LOOP('',(#5153));
#1516=EDGE_LOOP('',(#5154,#5155,#5156,#5157,#5158,#5159));
#1517=EDGE_LOOP('',(#5160));
#1937=LINE('',#10042,#2401);
#1938=LINE('',#10047,#2402);
#1939=LINE('',#10053,#2403);
#1940=LINE('',#10079,#2404);
#1941=LINE('',#10081,#2405);
#1942=LINE('',#10082,#2406);
#1943=LINE('',#10085,#2407);
#1944=LINE('',#10086,#2408);
#1945=LINE('',#10089,#2409);
#1946=LINE('',#10090,#2410);
#1947=LINE('',#10093,#2411);
#1948=LINE('',#10094,#2412);
#1949=LINE('',#10097,#2413);
#1950=LINE('',#10098,#2414);
#1951=LINE('',#10100,#2415);
#2401=VECTOR('',#8303,0.3);
#2402=VECTOR('',#8310,0.27);
#2403=VECTOR('',#8317,0.576175134594813);
#2404=VECTOR('',#8320,1.);
#2405=VECTOR('',#8321,1.);
#2406=VECTOR('',#8322,1.);
#2407=VECTOR('',#8325,1.);
#2408=VECTOR('',#8326,1.);
#2409=VECTOR('',#8329,1.);
#2410=VECTOR('',#8330,1.);
#2411=VECTOR('',#8333,1.);
#2412=VECTOR('',#8334,1.);
#2413=VECTOR('',#8337,1.);
#2414=VECTOR('',#8338,1.);
#2415=VECTOR('',#8341,1.);
#2730=CIRCLE('',#6751,0.2942);
#2731=CIRCLE('',#6752,0.2942);
#2732=CIRCLE('',#6754,0.24);
#2733=CIRCLE('',#6757,0.475);
#3141=VERTEX_POINT('',#10039);
#3142=VERTEX_POINT('',#10041);
#3143=VERTEX_POINT('',#10045);
#3144=VERTEX_POINT('',#10050);
#3145=VERTEX_POINT('',#10052);
#3146=VERTEX_POINT('',#10054);
#3147=VERTEX_POINT('',#10058);
#3148=VERTEX_POINT('',#10062);
#3149=VERTEX_POINT('',#10066);
#3150=VERTEX_POINT('',#10070);
#3151=VERTEX_POINT('',#10078);
#3152=VERTEX_POINT('',#10080);
#3153=VERTEX_POINT('',#10084);
#3154=VERTEX_POINT('',#10088);
#3155=VERTEX_POINT('',#10092);
#3156=VERTEX_POINT('',#10096);
#3813=EDGE_CURVE('',#3141,#3141,#2730,.F.);
#3814=EDGE_CURVE('',#3141,#3142,#1937,.T.);
#3815=EDGE_CURVE('',#3142,#3142,#2731,.F.);
#3816=EDGE_CURVE('',#3143,#3143,#2732,.T.);
#3817=EDGE_CURVE('',#3143,#3141,#1938,.T.);
#3818=EDGE_CURVE('',#3144,#3144,#2733,.T.);
#3819=EDGE_CURVE('',#3144,#3145,#1939,.T.);
#3820=EDGE_CURVE('',#3146,#3145,#245,.T.);
#3821=EDGE_CURVE('',#3147,#3146,#246,.T.);
#3822=EDGE_CURVE('',#3148,#3147,#247,.T.);
#3823=EDGE_CURVE('',#3149,#3148,#248,.T.);
#3824=EDGE_CURVE('',#3150,#3149,#249,.T.);
#3825=EDGE_CURVE('',#3145,#3150,#250,.T.);
#3826=EDGE_CURVE('',#3151,#3149,#1940,.T.);
#3827=EDGE_CURVE('',#3151,#3152,#1941,.T.);
#3828=EDGE_CURVE('',#3152,#3150,#1942,.T.);
#3829=EDGE_CURVE('',#3153,#3148,#1943,.T.);
#3830=EDGE_CURVE('',#3153,#3151,#1944,.T.);
#3831=EDGE_CURVE('',#3154,#3147,#1945,.T.);
#3832=EDGE_CURVE('',#3154,#3153,#1946,.T.);
#3833=EDGE_CURVE('',#3155,#3146,#1947,.T.);
#3834=EDGE_CURVE('',#3155,#3154,#1948,.T.);
#3835=EDGE_CURVE('',#3156,#3145,#1949,.T.);
#3836=EDGE_CURVE('',#3156,#3155,#1950,.T.);
#3837=EDGE_CURVE('',#3152,#3156,#1951,.T.);
#5111=ORIENTED_EDGE('',*,*,#3813,.F.);
#5112=ORIENTED_EDGE('',*,*,#3814,.T.);
#5113=ORIENTED_EDGE('',*,*,#3815,.F.);
#5114=ORIENTED_EDGE('',*,*,#3814,.F.);
#5115=ORIENTED_EDGE('',*,*,#3816,.F.);
#5116=ORIENTED_EDGE('',*,*,#3817,.T.);
#5117=ORIENTED_EDGE('',*,*,#3813,.T.);
#5118=ORIENTED_EDGE('',*,*,#3817,.F.);
#5119=ORIENTED_EDGE('',*,*,#3816,.T.);
#5120=ORIENTED_EDGE('',*,*,#3818,.F.);
#5121=ORIENTED_EDGE('',*,*,#3819,.T.);
#5122=ORIENTED_EDGE('',*,*,#3820,.F.);
#5123=ORIENTED_EDGE('',*,*,#3821,.F.);
#5124=ORIENTED_EDGE('',*,*,#3822,.F.);
#5125=ORIENTED_EDGE('',*,*,#3823,.F.);
#5126=ORIENTED_EDGE('',*,*,#3824,.F.);
#5127=ORIENTED_EDGE('',*,*,#3825,.F.);
#5128=ORIENTED_EDGE('',*,*,#3819,.F.);
#5129=ORIENTED_EDGE('',*,*,#3824,.T.);
#5130=ORIENTED_EDGE('',*,*,#3826,.F.);
#5131=ORIENTED_EDGE('',*,*,#3827,.T.);
#5132=ORIENTED_EDGE('',*,*,#3828,.T.);
#5133=ORIENTED_EDGE('',*,*,#3823,.T.);
#5134=ORIENTED_EDGE('',*,*,#3829,.F.);
#5135=ORIENTED_EDGE('',*,*,#3830,.T.);
#5136=ORIENTED_EDGE('',*,*,#3826,.T.);
#5137=ORIENTED_EDGE('',*,*,#3822,.T.);
#5138=ORIENTED_EDGE('',*,*,#3831,.F.);
#5139=ORIENTED_EDGE('',*,*,#3832,.T.);
#5140=ORIENTED_EDGE('',*,*,#3829,.T.);
#5141=ORIENTED_EDGE('',*,*,#3821,.T.);
#5142=ORIENTED_EDGE('',*,*,#3833,.F.);
#5143=ORIENTED_EDGE('',*,*,#3834,.T.);
#5144=ORIENTED_EDGE('',*,*,#3831,.T.);
#5145=ORIENTED_EDGE('',*,*,#3820,.T.);
#5146=ORIENTED_EDGE('',*,*,#3835,.F.);
#5147=ORIENTED_EDGE('',*,*,#3836,.T.);
#5148=ORIENTED_EDGE('',*,*,#3833,.T.);
#5149=ORIENTED_EDGE('',*,*,#3825,.T.);
#5150=ORIENTED_EDGE('',*,*,#3828,.F.);
#5151=ORIENTED_EDGE('',*,*,#3837,.T.);
#5152=ORIENTED_EDGE('',*,*,#3835,.T.);
#5153=ORIENTED_EDGE('',*,*,#3818,.T.);
#5154=ORIENTED_EDGE('',*,*,#3832,.F.);
#5155=ORIENTED_EDGE('',*,*,#3834,.F.);
#5156=ORIENTED_EDGE('',*,*,#3836,.F.);
#5157=ORIENTED_EDGE('',*,*,#3837,.F.);
#5158=ORIENTED_EDGE('',*,*,#3827,.F.);
#5159=ORIENTED_EDGE('',*,*,#3830,.F.);
#5160=ORIENTED_EDGE('',*,*,#3815,.T.);
#5520=CYLINDRICAL_SURFACE('',#6750,0.2942);
#5806=ADVANCED_FACE('',(#1033),#5520,.T.);
#5807=ADVANCED_FACE('',(#1034),#281,.T.);
#5808=ADVANCED_FACE('',(#1035),#692,.T.);
#5809=ADVANCED_FACE('',(#1036),#282,.T.);
#5810=ADVANCED_FACE('',(#1037),#693,.T.);
#5811=ADVANCED_FACE('',(#1038),#694,.T.);
#5812=ADVANCED_FACE('',(#1039),#695,.T.);
#5813=ADVANCED_FACE('',(#1040),#696,.T.);
#5814=ADVANCED_FACE('',(#1041),#697,.T.);
#5815=ADVANCED_FACE('',(#1042),#698,.T.);
#5816=ADVANCED_FACE('',(#1043),#699,.T.);
#5817=ADVANCED_FACE('',(#1044,#516),#700,.F.);
#5907=CLOSED_SHELL('',(#5806,#5807,#5808,#5809,#5810,#5811,#5812,#5813,
#5814,#5815,#5816,#5817));
#6749=AXIS2_PLACEMENT_3D('',#10037,#8297,#8298);
#6750=AXIS2_PLACEMENT_3D('',#10038,#8299,#8300);
#6751=AXIS2_PLACEMENT_3D('',#10040,#8301,#8302);
#6752=AXIS2_PLACEMENT_3D('',#10043,#8304,#8305);
#6753=AXIS2_PLACEMENT_3D('',#10044,#8306,#8307);
#6754=AXIS2_PLACEMENT_3D('',#10046,#8308,#8309);
#6755=AXIS2_PLACEMENT_3D('',#10048,#8311,#8312);
#6756=AXIS2_PLACEMENT_3D('',#10049,#8313,#8314);
#6757=AXIS2_PLACEMENT_3D('',#10051,#8315,#8316);
#6758=AXIS2_PLACEMENT_3D('',#10077,#8318,#8319);
#6759=AXIS2_PLACEMENT_3D('',#10083,#8323,#8324);
#6760=AXIS2_PLACEMENT_3D('',#10087,#8327,#8328);
#6761=AXIS2_PLACEMENT_3D('',#10091,#8331,#8332);
#6762=AXIS2_PLACEMENT_3D('',#10095,#8335,#8336);
#6763=AXIS2_PLACEMENT_3D('',#10099,#8339,#8340);
#6764=AXIS2_PLACEMENT_3D('',#10101,#8342,#8343);
#6765=AXIS2_PLACEMENT_3D('',#10102,#8344,#8345);
#8297=DIRECTION('axis',(0.,0.,1.));
#8298=DIRECTION('refdir',(1.,0.,0.));
#8299=DIRECTION('center_axis',(0.,-1.,0.));
#8300=DIRECTION('ref_axis',(1.,0.,0.));
#8301=DIRECTION('center_axis',(0.,1.,0.));
#8302=DIRECTION('ref_axis',(1.,0.,0.));
#8303=DIRECTION('',(0.,1.,0.));
#8304=DIRECTION('center_axis',(0.,-1.,0.));
#8305=DIRECTION('ref_axis',(1.,0.,0.));
#8306=DIRECTION('center_axis',(0.,1.,0.));
#8307=DIRECTION('ref_axis',(1.,0.,0.));
#8308=DIRECTION('center_axis',(0.,-1.,0.));
#8309=DIRECTION('ref_axis',(1.,0.,0.));
#8310=DIRECTION('',(-0.707106781186547,0.707106781186548,-8.65956056235493E-17));
#8311=DIRECTION('center_axis',(0.,-1.,0.));
#8312=DIRECTION('ref_axis',(0.,0.,-1.));
#8313=DIRECTION('center_axis',(0.,-1.,0.));
#8314=DIRECTION('ref_axis',(1.,0.,0.));
#8315=DIRECTION('center_axis',(0.,1.,0.));
#8316=DIRECTION('ref_axis',(1.,0.,0.));
#8317=DIRECTION('',(-0.866025403784439,-0.5,-1.06057523872491E-16));
#8318=DIRECTION('center_axis',(1.92296268638356E-16,0.,-1.));
#8319=DIRECTION('ref_axis',(-1.,0.,-1.92296268638356E-16));
#8320=DIRECTION('',(0.,1.,0.));
#8321=DIRECTION('',(-1.,0.,-1.92296268638356E-16));
#8322=DIRECTION('',(0.,1.,0.));
#8323=DIRECTION('center_axis',(0.866025403784439,0.,-0.5));
#8324=DIRECTION('ref_axis',(-0.5,0.,-0.866025403784439));
#8325=DIRECTION('',(0.,1.,0.));
#8326=DIRECTION('',(-0.5,0.,-0.866025403784439));
#8327=DIRECTION('center_axis',(0.866025403784439,0.,0.5));
#8328=DIRECTION('ref_axis',(0.5,0.,-0.866025403784439));
#8329=DIRECTION('',(0.,1.,0.));
#8330=DIRECTION('',(0.5,0.,-0.866025403784439));
#8331=DIRECTION('center_axis',(-1.92296268638356E-16,0.,1.));
#8332=DIRECTION('ref_axis',(1.,0.,1.92296268638356E-16));
#8333=DIRECTION('',(0.,1.,0.));
#8334=DIRECTION('',(1.,0.,1.92296268638356E-16));
#8335=DIRECTION('center_axis',(-0.866025403784439,0.,0.5));
#8336=DIRECTION('ref_axis',(0.5,0.,0.866025403784439));
#8337=DIRECTION('',(0.,1.,0.));
#8338=DIRECTION('',(0.5,0.,0.866025403784439));
#8339=DIRECTION('center_axis',(-0.866025403784439,0.,-0.5));
#8340=DIRECTION('ref_axis',(-0.5,0.,0.866025403784439));
#8341=DIRECTION('',(-0.5,0.,0.866025403784438));
#8342=DIRECTION('center_axis',(0.,1.,0.));
#8343=DIRECTION('ref_axis',(0.,0.,1.));
#8344=DIRECTION('center_axis',(0.,1.,0.));
#8345=DIRECTION('ref_axis',(1.,0.,0.));
#10037=CARTESIAN_POINT('',(0.,0.,0.));
#10038=CARTESIAN_POINT('Origin',(0.,-1.445,0.));
#10039=CARTESIAN_POINT('',(-0.2942,-2.9458,3.60291088309151E-17));
#10040=CARTESIAN_POINT('Origin',(0.,-2.9458,0.));
#10041=CARTESIAN_POINT('',(-0.2942,0.,-3.60291088309151E-17));
#10042=CARTESIAN_POINT('',(-0.2942,-1.445,-3.60291088309151E-17));
#10043=CARTESIAN_POINT('Origin',(0.,0.,0.));
#10044=CARTESIAN_POINT('Origin',(0.,-2.97,0.));
#10045=CARTESIAN_POINT('',(-0.24,-3.,-2.93915231795365E-17));
#10046=CARTESIAN_POINT('Origin',(0.,-3.,0.));
#10047=CARTESIAN_POINT('',(-0.27,-2.97,-3.30654635769785E-17));
#10048=CARTESIAN_POINT('Origin',(0.,-3.,0.));
#10049=CARTESIAN_POINT('Origin',(0.,0.341586508806388,0.));
#10050=CARTESIAN_POINT('',(-0.475,0.4,-5.81707229594993E-17));
#10051=CARTESIAN_POINT('Origin',(0.,0.4,0.));
#10052=CARTESIAN_POINT('',(-0.577350269189626,0.340908044531739,-7.07050159149938E-17));
#10053=CARTESIAN_POINT('',(-0.576175134594813,0.341586508806388,-7.05611034329833E-17));
#10054=CARTESIAN_POINT('',(-0.288675134594813,0.340908044531739,0.5));
#10055=CARTESIAN_POINT('Ctrl Pts',(-0.288675134594813,0.340908044531739,
0.5));
#10056=CARTESIAN_POINT('Ctrl Pts',(-0.433012701893303,0.424241377863696,
0.249999999998124));
#10057=CARTESIAN_POINT('Ctrl Pts',(-0.577350269189626,0.340908044531739,
-7.07050159149938E-17));
#10058=CARTESIAN_POINT('',(0.288675134594813,0.340908044531739,0.5));
#10059=CARTESIAN_POINT('Ctrl Pts',(0.288675134594813,0.340908044531739,
0.5));
#10060=CARTESIAN_POINT('Ctrl Pts',(-2.16648921025353E-12,0.424241377863696,
0.5));
#10061=CARTESIAN_POINT('Ctrl Pts',(-0.288675134594813,0.340908044531739,
0.5));
#10062=CARTESIAN_POINT('',(0.577350269189626,0.340908044531739,0.));
#10063=CARTESIAN_POINT('Ctrl Pts',(0.577350269189626,0.340908044531739,
0.));
#10064=CARTESIAN_POINT('Ctrl Pts',(0.433012701891136,0.424241377863697,
0.250000000001876));
#10065=CARTESIAN_POINT('Ctrl Pts',(0.288675134594813,0.340908044531739,
0.5));
#10066=CARTESIAN_POINT('',(0.288675134594813,0.340908044531739,-0.5));
#10067=CARTESIAN_POINT('Ctrl Pts',(0.288675134594813,0.340908044531739,
-0.5));
#10068=CARTESIAN_POINT('Ctrl Pts',(0.433012701893303,0.424241377863696,
-0.249999999998124));
#10069=CARTESIAN_POINT('Ctrl Pts',(0.577350269189626,0.340908044531739,
0.));
#10070=CARTESIAN_POINT('',(-0.288675134594813,0.340908044531739,-0.5));
#10071=CARTESIAN_POINT('Ctrl Pts',(-0.288675134594813,0.340908044531739,
-0.5));
#10072=CARTESIAN_POINT('Ctrl Pts',(2.16660023255599E-12,0.424241377863696,
-0.5));
#10073=CARTESIAN_POINT('Ctrl Pts',(0.288675134594813,0.340908044531739,
-0.5));
#10074=CARTESIAN_POINT('Ctrl Pts',(-0.577350269189626,0.340908044531739,
-7.07050159149938E-17));
#10075=CARTESIAN_POINT('Ctrl Pts',(-0.433012701891136,0.424241377863697,
-0.250000000001876));
#10076=CARTESIAN_POINT('Ctrl Pts',(-0.288675134594813,0.340908044531739,
-0.5));
#10077=CARTESIAN_POINT('Origin',(0.288675134594813,0.,-0.5));
#10078=CARTESIAN_POINT('',(0.288675134594813,0.,-0.5));
#10079=CARTESIAN_POINT('',(0.288675134594813,0.,-0.5));
#10080=CARTESIAN_POINT('',(-0.288675134594813,0.,-0.5));
#10081=CARTESIAN_POINT('',(0.288675134594813,0.,-0.5));
#10082=CARTESIAN_POINT('',(-0.288675134594813,0.,-0.5));
#10083=CARTESIAN_POINT('Origin',(0.577350269189626,0.,0.));
#10084=CARTESIAN_POINT('',(0.577350269189626,0.,0.));
#10085=CARTESIAN_POINT('',(0.577350269189626,0.,0.));
#10086=CARTESIAN_POINT('',(0.577350269189626,0.,0.));
#10087=CARTESIAN_POINT('Origin',(0.288675134594813,0.,0.5));
#10088=CARTESIAN_POINT('',(0.288675134594813,0.,0.5));
#10089=CARTESIAN_POINT('',(0.288675134594813,0.,0.5));
#10090=CARTESIAN_POINT('',(0.288675134594813,0.,0.5));
#10091=CARTESIAN_POINT('Origin',(-0.288675134594813,0.,0.5));
#10092=CARTESIAN_POINT('',(-0.288675134594813,0.,0.5));
#10093=CARTESIAN_POINT('',(-0.288675134594813,0.,0.5));
#10094=CARTESIAN_POINT('',(-0.288675134594813,0.,0.5));
#10095=CARTESIAN_POINT('Origin',(-0.577350269189626,0.,-7.07050159149938E-17));
#10096=CARTESIAN_POINT('',(-0.577350269189626,0.,-7.07050159149938E-17));
#10097=CARTESIAN_POINT('',(-0.577350269189626,0.,-7.07050159149938E-17));
#10098=CARTESIAN_POINT('',(-0.577350269189626,0.,-7.07050159149938E-17));
#10099=CARTESIAN_POINT('Origin',(-0.288675134594813,0.,-0.5));
#10100=CARTESIAN_POINT('',(-0.288675134594813,0.,-0.5));
#10101=CARTESIAN_POINT('Origin',(0.,0.4,0.));
#10102=CARTESIAN_POINT('Origin',(0.,0.,0.));
#10476=UNCERTAINTY_MEASURE_WITH_UNIT(LENGTH_MEASURE(0.001),#10518,
'DISTANCE_ACCURACY_VALUE',
'Maximum model space distance between geometric entities at asserted c
onnectivities');
#10484=UNCERTAINTY_MEASURE_WITH_UNIT(LENGTH_MEASURE(0.001),#10518,
'DISTANCE_ACCURACY_VALUE',
'Maximum model space distance between geometric entities at asserted c
onnectivities');
#10509=(
GEOMETRIC_REPRESENTATION_CONTEXT(3)
GLOBAL_UNCERTAINTY_ASSIGNED_CONTEXT((#10476))
GLOBAL_UNIT_ASSIGNED_CONTEXT((#10518,#10520,#10521))
REPRESENTATION_CONTEXT('','3D')
);
#10517=(
GEOMETRIC_REPRESENTATION_CONTEXT(3)
GLOBAL_UNCERTAINTY_ASSIGNED_CONTEXT((#10484))
GLOBAL_UNIT_ASSIGNED_CONTEXT((#10518,#10520,#10521))
REPRESENTATION_CONTEXT('','3D')
);
#10518=(
LENGTH_UNIT()
NAMED_UNIT(*)
SI_UNIT(.CENTI.,.METRE.)
);
#10520=(
NAMED_UNIT(*)
PLANE_ANGLE_UNIT()
SI_UNIT($,.RADIAN.)
);
#10521=(
NAMED_UNIT(*)
SI_UNIT($,.STERADIAN.)
SOLID_ANGLE_UNIT()
);
#10546=SHAPE_DEFINITION_REPRESENTATION(#10578,#10665);
#10578=PRODUCT_DEFINITION_SHAPE('',$,#10698);
#10665=SHAPE_REPRESENTATION('',(#6749),#10509);
#10673=PRODUCT_DEFINITION_CONTEXT('part definition',#10771,'design');
#10698=PRODUCT_DEFINITION('Hex Bolt - M6 x 30 mm',
'Hex Bolt - M6 x 30 mm',#10730,#10673);
#10730=PRODUCT_DEFINITION_FORMATION('',$,#10797);
#10771=APPLICATION_CONTEXT(
'Core Data for Automotive Mechanical Design Process');
#10772=PRODUCT_CONTEXT('part definition',#10771,'mechanical');
#10797=PRODUCT('Hex Bolt - M6 x 30 mm','Hex Bolt - M6 x 30 mm',
'Hex Bolt - M6 x 30 mm',(#10772));
#10875=COLOUR_RGB('Black',0.12,0.14,0.17);
#10876=FILL_AREA_STYLE_COLOUR('',#10875);
#10877=FILL_AREA_STYLE('',(#10876));
#10878=SURFACE_STYLE_FILL_AREA(#10877);
#10879=SURFACE_SIDE_STYLE('',(#10878));
#10880=SURFACE_STYLE_USAGE(.BOTH.,#10879);
#10881=PRESENTATION_STYLE_ASSIGNMENT((#10880));
ENDSEC;
END-ISO-10303-21;
